ISO-10303-21;
HEADER;
/* Generated by software containing ST-Developer
 * from STEP Tools, Inc. (www.steptools.com) 
 */

FILE_DESCRIPTION(
/* description */ ('PAT-054'),
/* implementation_level */ '2;1');

FILE_NAME(
/* name */ 'Socket Set Screw - M5x8.step',
/* time_stamp */ '2026-10-29T16:38:13-07:00',
/* author */ (''),
/* organization */ (''),
/* preprocessor_version */ 'ST-DEVELOPER v20.2',
/* originating_system */ 'Autodesk Translation Framework v15.17.0.0',
/* authorisation */ '');

FILE_SCHEMA (('AUTOMOTIVE_DESIGN { 1 0 10303 214 3 1 1 }'));
ENDSEC;

DATA;
#10=MECHANICAL_DESIGN_GEOMETRIC_PRESENTATION_REPRESENTATION('',(#955),#33981);
#801=CONICAL_SURFACE('',#14787,0.235,0.785398163397448);
#802=CONICAL_SURFACE('',#14791,0.2125,0.785398163397448);
#852=SHAPE_REPRESENTATION_RELATIONSHIP('SRR','None',#34230,#896);
#896=ADVANCED_BREP_SHAPE_REPRESENTATION('',(#1010),#33978);
#955=STYLED_ITEM('',(#34524),#1010);
#1010=MANIFOLD_SOLID_BREP('Body1',#13070);
#1224=FACE_BOUND('',#3208,.T.);
#1553=PLANE('',#14778);
#1554=PLANE('',#14779);
#1555=PLANE('',#14780);
#1556=PLANE('',#14781);
#1557=PLANE('',#14782);
#1558=PLANE('',#14783);
#1559=PLANE('',#14784);
#1560=PLANE('',#14785);
#1561=PLANE('',#14793);
#2265=FACE_OUTER_BOUND('',#3200,.T.);
#2266=FACE_OUTER_BOUND('',#3201,.T.);
#2267=FACE_OUTER_BOUND('',#3202,.T.);
#2268=FACE_OUTER_BOUND('',#3203,.T.);
#2269=FACE_OUTER_BOUND('',#3204,.T.);
#2270=FACE_OUTER_BOUND('',#3205,.T.);
#2271=FACE_OUTER_BOUND('',#3206,.T.);
#2272=FACE_OUTER_BOUND('',#3207,.T.);
#2273=FACE_OUTER_BOUND('',#3209,.T.);
#2274=FACE_OUTER_BOUND('',#3210,.T.);
#2275=FACE_OUTER_BOUND('',#3211,.T.);
#2276=FACE_OUTER_BOUND('',#3212,.T.);
#3200=EDGE_LOOP('',(#11853,#11854,#11855,#11856));
#3201=EDGE_LOOP('',(#11857,#11858,#11859,#11860));
#3202=EDGE_LOOP('',(#11861,#11862,#11863,#11864));
#3203=EDGE_LOOP('',(#11865,#11866,#11867,#11868));
#3204=EDGE_LOOP('',(#11869,#11870,#11871,#11872));
#3205=EDGE_LOOP('',(#11873,#11874,#11875,#11876));
#3206=EDGE_LOOP('',(#11877,#11878,#11879,#11880,#11881,#11882));
#3207=EDGE_LOOP('',(#11883));
#3208=EDGE_LOOP('',(#11884,#11885,#11886,#11887,#11888,#11889));
#3209=EDGE_LOOP('',(#11890,#11891,#11892,#11893));
#3210=EDGE_LOOP('',(#11894,#11895,#11896,#11897));
#3211=EDGE_LOOP('',(#11898,#11899,#11900,#11901));
#3212=EDGE_LOOP('',(#11902));
#4124=LINE('',#33682,#5058);
#4125=LINE('',#33684,#5059);
#4126=LINE('',#33686,#5060);
#4127=LINE('',#33687,#5061);
#4128=LINE('',#33690,#5062);
#4129=LINE('',#33692,#5063);
#4130=LINE('',#33693,#5064);
#4131=LINE('',#33696,#5065);
#4132=LINE('',#33698,#5066);
#4133=LINE('',#33699,#5067);
#4134=LINE('',#33702,#5068);
#4135=LINE('',#33704,#5069);
#4136=LINE('',#33705,#5070);
#4137=LINE('',#33708,#5071);
#4138=LINE('',#33710,#5072);
#4139=LINE('',#33711,#5073);
#4140=LINE('',#33713,#5074);
#4141=LINE('',#33714,#5075);
#4142=LINE('',#33722,#5076);
#4143=LINE('',#33726,#5077);
#4144=LINE('',#33730,#5078);
#5058=VECTOR('',#18217,1.);
#5059=VECTOR('',#18218,1.);
#5060=VECTOR('',#18219,1.);
#5061=VECTOR('',#18220,1.);
#5062=VECTOR('',#18223,1.);
#5063=VECTOR('',#18224,1.);
#5064=VECTOR('',#18225,1.);
#5065=VECTOR('',#18228,1.);
#5066=VECTOR('',#18229,1.);
#5067=VECTOR('',#18230,1.);
#5068=VECTOR('',#18233,1.);
#5069=VECTOR('',#18234,1.);
#5070=VECTOR('',#18235,1.);
#5071=VECTOR('',#18238,1.);
#5072=VECTOR('',#18239,1.);
#5073=VECTOR('',#18240,1.);
#5074=VECTOR('',#18243,1.);
#5075=VECTOR('',#18244,1.);
#5076=VECTOR('',#18255,0.235);
#5077=VECTOR('',#18260,0.25);
#5078=VECTOR('',#18265,0.2125);
#5554=CIRCLE('',#14786,0.22);
#5555=CIRCLE('',#14788,0.24505);
#5556=CIRCLE('',#14790,0.24505);
#5557=CIRCLE('',#14792,0.175);
#6704=VERTEX_POINT('',#33680);
#6705=VERTEX_POINT('',#33681);
#6706=VERTEX_POINT('',#33683);
#6707=VERTEX_POINT('',#33685);
#6708=VERTEX_POINT('',#33689);
#6709=VERTEX_POINT('',#33691);
#6710=VERTEX_POINT('',#33695);
#6711=VERTEX_POINT('',#33697);
#6712=VERTEX_POINT('',#33701);
#6713=VERTEX_POINT('',#33703);
#6714=VERTEX_POINT('',#33707);
#6715=VERTEX_POINT('',#33709);
#6716=VERTEX_POINT('',#33717);
#6717=VERTEX_POINT('',#33720);
#6718=VERTEX_POINT('',#33724);
#6719=VERTEX_POINT('',#33728);
#8426=EDGE_CURVE('',#6704,#6705,#4124,.T.);
#8427=EDGE_CURVE('',#6704,#6706,#4125,.T.);
#8428=EDGE_CURVE('',#6706,#6707,#4126,.T.);
#8429=EDGE_CURVE('',#6705,#6707,#4127,.T.);
#8430=EDGE_CURVE('',#6708,#6704,#4128,.T.);
#8431=EDGE_CURVE('',#6708,#6709,#4129,.T.);
#8432=EDGE_CURVE('',#6709,#6706,#4130,.T.);
#8433=EDGE_CURVE('',#6710,#6708,#4131,.T.);
#8434=EDGE_CURVE('',#6710,#6711,#4132,.T.);
#8435=EDGE_CURVE('',#6711,#6709,#4133,.T.);
#8436=EDGE_CURVE('',#6712,#6710,#4134,.T.);
#8437=EDGE_CURVE('',#6712,#6713,#4135,.T.);
#8438=EDGE_CURVE('',#6713,#6711,#4136,.T.);
#8439=EDGE_CURVE('',#6714,#6712,#4137,.T.);
#8440=EDGE_CURVE('',#6714,#6715,#4138,.T.);
#8441=EDGE_CURVE('',#6715,#6713,#4139,.T.);
#8442=EDGE_CURVE('',#6705,#6714,#4140,.T.);
#8443=EDGE_CURVE('',#6707,#6715,#4141,.T.);
#8444=EDGE_CURVE('',#6716,#6716,#5554,.T.);
#8445=EDGE_CURVE('',#6717,#6717,#5555,.T.);
#8446=EDGE_CURVE('',#6717,#6716,#4142,.T.);
#8447=EDGE_CURVE('',#6718,#6718,#5556,.F.);
#8448=EDGE_CURVE('',#6718,#6717,#4143,.T.);
#8449=EDGE_CURVE('',#6719,#6719,#5557,.T.);
#8450=EDGE_CURVE('',#6719,#6718,#4144,.T.);
#11853=ORIENTED_EDGE('',*,*,#8426,.F.);
#11854=ORIENTED_EDGE('',*,*,#8427,.T.);
#11855=ORIENTED_EDGE('',*,*,#8428,.T.);
#11856=ORIENTED_EDGE('',*,*,#8429,.F.);
#11857=ORIENTED_EDGE('',*,*,#8430,.F.);
#11858=ORIENTED_EDGE('',*,*,#8431,.T.);
#11859=ORIENTED_EDGE('',*,*,#8432,.T.);
#11860=ORIENTED_EDGE('',*,*,#8427,.F.);
#11861=ORIENTED_EDGE('',*,*,#8433,.F.);
#11862=ORIENTED_EDGE('',*,*,#8434,.T.);
#11863=ORIENTED_EDGE('',*,*,#8435,.T.);
#11864=ORIENTED_EDGE('',*,*,#8431,.F.);
#11865=ORIENTED_EDGE('',*,*,#8436,.F.);
#11866=ORIENTED_EDGE('',*,*,#8437,.T.);
#11867=ORIENTED_EDGE('',*,*,#8438,.T.);
#11868=ORIENTED_EDGE('',*,*,#8434,.F.);
#11869=ORIENTED_EDGE('',*,*,#8439,.F.);
#11870=ORIENTED_EDGE('',*,*,#8440,.T.);
#11871=ORIENTED_EDGE('',*,*,#8441,.T.);
#11872=ORIENTED_EDGE('',*,*,#8437,.F.);
#11873=ORIENTED_EDGE('',*,*,#8442,.F.);
#11874=ORIENTED_EDGE('',*,*,#8429,.T.);
#11875=ORIENTED_EDGE('',*,*,#8443,.T.);
#11876=ORIENTED_EDGE('',*,*,#8440,.F.);
#11877=ORIENTED_EDGE('',*,*,#8443,.F.);
#11878=ORIENTED_EDGE('',*,*,#8428,.F.);
#11879=ORIENTED_EDGE('',*,*,#8432,.F.);
#11880=ORIENTED_EDGE('',*,*,#8435,.F.);
#11881=ORIENTED_EDGE('',*,*,#8438,.F.);
#11882=ORIENTED_EDGE('',*,*,#8441,.F.);
#11883=ORIENTED_EDGE('',*,*,#8444,.F.);
#11884=ORIENTED_EDGE('',*,*,#8426,.T.);
#11885=ORIENTED_EDGE('',*,*,#8442,.T.);
#11886=ORIENTED_EDGE('',*,*,#8439,.T.);
#11887=ORIENTED_EDGE('',*,*,#8436,.T.);
#11888=ORIENTED_EDGE('',*,*,#8433,.T.);
#11889=ORIENTED_EDGE('',*,*,#8430,.T.);
#11890=ORIENTED_EDGE('',*,*,#8445,.F.);
#11891=ORIENTED_EDGE('',*,*,#8446,.T.);
#11892=ORIENTED_EDGE('',*,*,#8444,.T.);
#11893=ORIENTED_EDGE('',*,*,#8446,.F.);
#11894=ORIENTED_EDGE('',*,*,#8447,.F.);
#11895=ORIENTED_EDGE('',*,*,#8448,.T.);
#11896=ORIENTED_EDGE('',*,*,#8445,.T.);
#11897=ORIENTED_EDGE('',*,*,#8448,.F.);
#11898=ORIENTED_EDGE('',*,*,#8449,.F.);
#11899=ORIENTED_EDGE('',*,*,#8450,.T.);
#11900=ORIENTED_EDGE('',*,*,#8447,.T.);
#11901=ORIENTED_EDGE('',*,*,#8450,.F.);
#11902=ORIENTED_EDGE('',*,*,#8449,.T.);
#12282=CYLINDRICAL_SURFACE('',#14789,0.24505);
#12977=ADVANCED_FACE('',(#2265),#1553,.F.);
#12978=ADVANCED_FACE('',(#2266),#1554,.F.);
#12979=ADVANCED_FACE('',(#2267),#1555,.F.);
#12980=ADVANCED_FACE('',(#2268),#1556,.F.);
#12981=ADVANCED_FACE('',(#2269),#1557,.F.);
#12982=ADVANCED_FACE('',(#2270),#1558,.F.);
#12983=ADVANCED_FACE('',(#2271),#1559,.F.);
#12984=ADVANCED_FACE('',(#2272,#1224),#1560,.T.);
#12985=ADVANCED_FACE('',(#2273),#801,.T.);
#12986=ADVANCED_FACE('',(#2274),#12282,.T.);
#12987=ADVANCED_FACE('',(#2275),#802,.T.);
#12988=ADVANCED_FACE('',(#2276),#1561,.T.);
#13070=CLOSED_SHELL('',(#12977,#12978,#12979,#12980,#12981,#12982,#12983,
#12984,#12985,#12986,#12987,#12988));
#14777=AXIS2_PLACEMENT_3D('',#33678,#18213,#18214);
#14778=AXIS2_PLACEMENT_3D('',#33679,#18215,#18216);
#14779=AXIS2_PLACEMENT_3D('',#33688,#18221,#18222);
#14780=AXIS2_PLACEMENT_3D('',#33694,#18226,#18227);
#14781=AXIS2_PLACEMENT_3D('',#33700,#18231,#18232);
#14782=AXIS2_PLACEMENT_3D('',#33706,#18236,#18237);
#14783=AXIS2_PLACEMENT_3D('',#33712,#18241,#18242);
#14784=AXIS2_PLACEMENT_3D('',#33715,#18245,#18246);
#14785=AXIS2_PLACEMENT_3D('',#33716,#18247,#18248);
#14786=AXIS2_PLACEMENT_3D('',#33718,#18249,#18250);
#14787=AXIS2_PLACEMENT_3D('',#33719,#18251,#18252);
#14788=AXIS2_PLACEMENT_3D('',#33721,#18253,#18254);
#14789=AXIS2_PLACEMENT_3D('',#33723,#18256,#18257);
#14790=AXIS2_PLACEMENT_3D('',#33725,#18258,#18259);
#14791=AXIS2_PLACEMENT_3D('',#33727,#18261,#18262);
#14792=AXIS2_PLACEMENT_3D('',#33729,#18263,#18264);
#14793=AXIS2_PLACEMENT_3D('',#33731,#18266,#18267);
#18213=DIRECTION('axis',(0.,0.,1.));
#18214=DIRECTION('refdir',(1.,0.,0.));
#18215=DIRECTION('center_axis',(0.866025403784439,0.,-0.5));
#18216=DIRECTION('ref_axis',(0.5,0.,0.866025403784439));
#18217=DIRECTION('',(0.5,0.,0.866025403784439));
#18218=DIRECTION('',(0.,-1.,0.));
#18219=DIRECTION('',(0.5,0.,0.866025403784439));
#18220=DIRECTION('',(0.,-1.,0.));
#18221=DIRECTION('center_axis',(1.92296268638356E-16,0.,-1.));
#18222=DIRECTION('ref_axis',(1.,0.,1.92296268638356E-16));
#18223=DIRECTION('',(1.,0.,1.92296268638356E-16));
#18224=DIRECTION('',(0.,-1.,0.));
#18225=DIRECTION('',(1.,0.,1.92296268638356E-16));
#18226=DIRECTION('center_axis',(-0.866025403784439,0.,-0.5));
#18227=DIRECTION('ref_axis',(0.5,0.,-0.866025403784439));
#18228=DIRECTION('',(0.5,0.,-0.866025403784439));
#18229=DIRECTION('',(0.,-1.,0.));
#18230=DIRECTION('',(0.5,0.,-0.866025403784438));
#18231=DIRECTION('center_axis',(-0.866025403784439,0.,0.5));
#18232=DIRECTION('ref_axis',(-0.5,0.,-0.866025403784439));
#18233=DIRECTION('',(-0.5,0.,-0.866025403784439));
#18234=DIRECTION('',(0.,-1.,0.));
#18235=DIRECTION('',(-0.5,0.,-0.866025403784439));
#18236=DIRECTION('center_axis',(-1.92296268638356E-16,0.,1.));
#18237=DIRECTION('ref_axis',(-1.,0.,-1.92296268638356E-16));
#18238=DIRECTION('',(-1.,0.,-1.92296268638356E-16));
#18239=DIRECTION('',(0.,-1.,0.));
#18240=DIRECTION('',(-1.,0.,-1.92296268638356E-16));
#18241=DIRECTION('center_axis',(0.866025403784439,0.,0.5));
#18242=DIRECTION('ref_axis',(-0.5,0.,0.866025403784439));
#18243=DIRECTION('',(-0.5,0.,0.866025403784439));
#18244=DIRECTION('',(-0.5,0.,0.866025403784439));
#18245=DIRECTION('center_axis',(0.,-1.,0.));
#18246=DIRECTION('ref_axis',(0.,0.,-1.));
#18247=DIRECTION('center_axis',(0.,1.,0.));
#18248=DIRECTION('ref_axis',(0.,0.,1.));
#18249=DIRECTION('center_axis',(0.,-1.,0.));
#18250=DIRECTION('ref_axis',(1.,0.,0.));
#18251=DIRECTION('center_axis',(0.,-1.,0.));
#18252=DIRECTION('ref_axis',(1.,0.,0.));
#18253=DIRECTION('center_axis',(0.,-1.,0.));
#18254=DIRECTION('ref_axis',(1.,0.,0.));
#18255=DIRECTION('',(0.707106781186547,0.707106781186548,8.65956056235493E-17));
#18256=DIRECTION('center_axis',(0.,-1.,0.));
#18257=DIRECTION('ref_axis',(1.,0.,0.));
#18258=DIRECTION('center_axis',(0.,1.,0.));
#18259=DIRECTION('ref_axis',(1.,0.,0.));
#18260=DIRECTION('',(0.,1.,0.));
#18261=DIRECTION('center_axis',(0.,1.,0.));
#18262=DIRECTION('ref_axis',(1.,0.,0.));
#18263=DIRECTION('center_axis',(0.,-1.,0.));
#18264=DIRECTION('ref_axis',(1.,0.,0.));
#18265=DIRECTION('',(-0.707106781186547,0.707106781186548,-8.65956056235493E-17));
#18266=DIRECTION('center_axis',(0.,-1.,0.));
#18267=DIRECTION('ref_axis',(0.,0.,-1.));
#33678=CARTESIAN_POINT('',(0.,0.,0.));
#33679=CARTESIAN_POINT('Origin',(0.0721687836487032,0.,-0.125));
#33680=CARTESIAN_POINT('',(0.0721687836487032,0.,-0.125));
#33681=CARTESIAN_POINT('',(0.144337567297406,0.,0.));
#33682=CARTESIAN_POINT('',(0.117710979560879,0.,-0.0461186027918559));
#33683=CARTESIAN_POINT('',(0.0721687836487032,-0.25,-0.125));
#33684=CARTESIAN_POINT('',(0.0721687836487032,0.,-0.125));
#33685=CARTESIAN_POINT('',(0.144337567297406,-0.25,0.));
#33686=CARTESIAN_POINT('',(0.144337567297406,-0.25,0.));
#33687=CARTESIAN_POINT('',(0.144337567297406,0.,0.));
#33688=CARTESIAN_POINT('Origin',(-0.0721687836487032,0.,-0.125));
#33689=CARTESIAN_POINT('',(-0.0721687836487032,0.,-0.125));
#33690=CARTESIAN_POINT('',(0.0739156081756484,0.,-0.125));
#33691=CARTESIAN_POINT('',(-0.0721687836487032,-0.25,-0.125));
#33692=CARTESIAN_POINT('',(-0.0721687836487032,0.,-0.125));
#33693=CARTESIAN_POINT('',(0.0721687836487032,-0.25,-0.125));
#33694=CARTESIAN_POINT('Origin',(-0.144337567297406,0.,-4.16333634234434E-17));
#33695=CARTESIAN_POINT('',(-0.144337567297406,0.,-1.76762539787485E-17));
#33696=CARTESIAN_POINT('',(-0.0987953713852306,0.,-0.0788813972081442));
#33697=CARTESIAN_POINT('',(-0.144337567297406,-0.25,-2.77555756156289E-17));
#33698=CARTESIAN_POINT('',(-0.144337567297406,0.,-1.76762539787485E-17));
#33699=CARTESIAN_POINT('',(-0.0721687836487032,-0.25,-0.125));
#33700=CARTESIAN_POINT('Origin',(-0.0721687836487033,0.,0.125));
#33701=CARTESIAN_POINT('',(-0.0721687836487033,0.,0.125));
#33702=CARTESIAN_POINT('',(-0.0627109795608791,0.,0.141381397208144));
#33703=CARTESIAN_POINT('',(-0.0721687836487033,-0.25,0.125));
#33704=CARTESIAN_POINT('',(-0.0721687836487033,0.,0.125));
#33705=CARTESIAN_POINT('',(-0.144337567297406,-0.25,-1.76762539787485E-17));
#33706=CARTESIAN_POINT('Origin',(0.0721687836487032,0.,0.125));
#33707=CARTESIAN_POINT('',(0.0721687836487032,0.,0.125));
#33708=CARTESIAN_POINT('',(0.146084391824352,0.,0.125));
#33709=CARTESIAN_POINT('',(0.0721687836487032,-0.25,0.125));
#33710=CARTESIAN_POINT('',(0.0721687836487032,0.,0.125));
#33711=CARTESIAN_POINT('',(-0.0721687836487033,-0.25,0.125));
#33712=CARTESIAN_POINT('Origin',(0.144337567297406,0.,0.));
#33713=CARTESIAN_POINT('',(0.153795371385231,0.,-0.0163813972081441));
#33714=CARTESIAN_POINT('',(0.0721687836487032,-0.25,0.125));
#33715=CARTESIAN_POINT('Origin',(0.,-0.25,0.));
#33716=CARTESIAN_POINT('Origin',(0.22,0.,0.));
#33717=CARTESIAN_POINT('',(-0.22,-8.67361737988404E-18,-2.69422295812418E-17));
#33718=CARTESIAN_POINT('Origin',(0.,0.,0.));
#33719=CARTESIAN_POINT('Origin',(0.,-0.015,0.));
#33720=CARTESIAN_POINT('',(-0.24505,-0.02505,-3.00099698131059E-17));
#33721=CARTESIAN_POINT('Origin',(0.,-0.02505,0.));
#33722=CARTESIAN_POINT('',(-0.235,-0.015,-2.87791997799628E-17));
#33723=CARTESIAN_POINT('Origin',(0.,-0.3775,0.));
#33724=CARTESIAN_POINT('',(-0.24505,-0.72995,3.00099698131059E-17));
#33725=CARTESIAN_POINT('Origin',(0.,-0.72995,0.));
#33726=CARTESIAN_POINT('',(-0.24505,-0.3775,-3.00099698131059E-17));
#33727=CARTESIAN_POINT('Origin',(0.,-0.7625,0.));
#33728=CARTESIAN_POINT('',(-0.175,-0.8,-2.14313189850787E-17));
#33729=CARTESIAN_POINT('Origin',(0.,-0.8,0.));
#33730=CARTESIAN_POINT('',(-0.2125,-0.7625,-2.60237444818813E-17));
#33731=CARTESIAN_POINT('Origin',(0.,-0.8,0.));
#33926=UNCERTAINTY_MEASURE_WITH_UNIT(LENGTH_MEASURE(0.001),#33982,
'DISTANCE_ACCURACY_VALUE',
'Maximum model space distance between geometric entities at asserted c
onnectivities');
#33929=UNCERTAINTY_MEASURE_WITH_UNIT(LENGTH_MEASURE(0.001),#33982,
'DISTANCE_ACCURACY_VALUE',
'Maximum model space distance between geometric entities at asserted c
onnectivities');
#33978=(
GEOMETRIC_REPRESENTATION_CONTEXT(3)
GLOBAL_UNCERTAINTY_ASSIGNED_CONTEXT((#33926))
GLOBAL_UNIT_ASSIGNED_CONTEXT((#33982,#33984,#33985))
REPRESENTATION_CONTEXT('','3D')
);
#33981=(
GEOMETRIC_REPRESENTATION_CONTEXT(3)
GLOBAL_UNCERTAINTY_ASSIGNED_CONTEXT((#33929))
GLOBAL_UNIT_ASSIGNED_CONTEXT((#33982,#33984,#33985))
REPRESENTATION_CONTEXT('','3D')
);
#33982=(
LENGTH_UNIT()
NAMED_UNIT(*)
SI_UNIT(.CENTI.,.METRE.)
);
#33984=(
NAMED_UNIT(*)
PLANE_ANGLE_UNIT()
SI_UNIT($,.RADIAN.)
);
#33985=(
NAMED_UNIT(*)
SI_UNIT($,.STERADIAN.)
SOLID_ANGLE_UNIT()
);
#34034=SHAPE_DEFINITION_REPRESENTATION(#34118,#34230);
#34118=PRODUCT_DEFINITION_SHAPE('',$,#34282);
#34230=SHAPE_REPRESENTATION('',(#14777),#33978);
#34233=PRODUCT_DEFINITION_CONTEXT('part definition',#34388,'design');
#34282=PRODUCT_DEFINITION('Socket Set Screw - M5x8',
'Socket Set Screw - M5x8',#34333,#34233);
#34333=PRODUCT_DEFINITION_FORMATION('',$,#34438);
#34388=APPLICATION_CONTEXT(
'Core Data for Automotive Mechanical Design Process');
#34389=PRODUCT_CONTEXT('part definition',#34388,'mechanical');
#34438=PRODUCT('Socket Set Screw - M5x8','Socket Set Screw - M5x8',
'Socket Set Screw - M5x8',(#34389));
#34518=COLOUR_RGB('Black',0.12,0.14,0.17);
#34519=FILL_AREA_STYLE_COLOUR('',#34518);
#34520=FILL_AREA_STYLE('',(#34519));
#34521=SURFACE_STYLE_FILL_AREA(#34520);
#34522=SURFACE_SIDE_STYLE('',(#34521));
#34523=SURFACE_STYLE_USAGE(.BOTH.,#34522);
#34524=PRESENTATION_STYLE_ASSIGNMENT((#34523));
ENDSEC;
END-ISO-10303-21;
